ISO-10303-21;
HEADER;
/* Generated by software containing ST-Developer
 * from STEP Tools, Inc. (www.steptools.com) 
 */

FILE_DESCRIPTION(
/* description */ ('Bearing friction torque test rig'),
/* implementation_level */ '2;1');

FILE_NAME(
/* name */ 'Support cap (3).step',
/* time_stamp */ '2026-10-28T03:24:04-07:00',
/* author */ (''),
/* organization */ (''),
/* preprocessor_version */ 'ST-DEVELOPER v20.2',
/* originating_system */ 'Autodesk Translation Framework v15.17.0.0',
/* authorisation */ '');

FILE_SCHEMA (('AUTOMOTIVE_DESIGN { 1 0 10303 214 3 1 1 }'));
ENDSEC;

DATA;
#10=MECHANICAL_DESIGN_GEOMETRIC_PRESENTATION_REPRESENTATION('',(#545),#14822);
#467=SHAPE_REPRESENTATION_RELATIONSHIP('SRR','None',#15006,#506);
#506=ADVANCED_BREP_SHAPE_REPRESENTATION('',(#599),#14786);
#545=STYLED_ITEM('',(#15277),#599);
#599=MANIFOLD_SOLID_BREP('Body1',#7661);
#733=FACE_BOUND('',#1729,.T.);
#734=FACE_BOUND('',#1733,.T.);
#735=FACE_BOUND('',#1734,.T.);
#736=FACE_BOUND('',#1735,.T.);
#737=FACE_BOUND('',#1736,.T.);
#738=FACE_BOUND('',#1737,.T.);
#739=FACE_BOUND('',#1739,.T.);
#740=FACE_BOUND('',#1740,.T.);
#741=FACE_BOUND('',#1741,.T.);
#742=FACE_BOUND('',#1742,.T.);
#743=FACE_BOUND('',#1743,.T.);
#911=PLANE('',#8370);
#912=PLANE('',#8377);
#913=PLANE('',#8378);
#1189=FACE_OUTER_BOUND('',#1723,.T.);
#1190=FACE_OUTER_BOUND('',#1724,.T.);
#1191=FACE_OUTER_BOUND('',#1725,.T.);
#1192=FACE_OUTER_BOUND('',#1726,.T.);
#1193=FACE_OUTER_BOUND('',#1727,.T.);
#1194=FACE_OUTER_BOUND('',#1728,.T.);
#1195=FACE_OUTER_BOUND('',#1730,.T.);
#1196=FACE_OUTER_BOUND('',#1731,.T.);
#1197=FACE_OUTER_BOUND('',#1732,.T.);
#1198=FACE_OUTER_BOUND('',#1738,.T.);
#1723=EDGE_LOOP('',(#5574,#5575,#5576,#5577));
#1724=EDGE_LOOP('',(#5578,#5579,#5580,#5581));
#1725=EDGE_LOOP('',(#5582,#5583,#5584,#5585));
#1726=EDGE_LOOP('',(#5586,#5587,#5588,#5589));
#1727=EDGE_LOOP('',(#5590,#5591,#5592,#5593));
#1728=EDGE_LOOP('',(#5594));
#1729=EDGE_LOOP('',(#5595));
#1730=EDGE_LOOP('',(#5596,#5597,#5598,#5599));
#1731=EDGE_LOOP('',(#5600,#5601,#5602,#5603));
#1732=EDGE_LOOP('',(#5604));
#1733=EDGE_LOOP('',(#5605));
#1734=EDGE_LOOP('',(#5606));
#1735=EDGE_LOOP('',(#5607));
#1736=EDGE_LOOP('',(#5608));
#1737=EDGE_LOOP('',(#5609));
#1738=EDGE_LOOP('',(#5610));
#1739=EDGE_LOOP('',(#5611));
#1740=EDGE_LOOP('',(#5612));
#1741=EDGE_LOOP('',(#5613));
#1742=EDGE_LOOP('',(#5614));
#1743=EDGE_LOOP('',(#5615));
#2318=LINE('',#12116,#2762);
#2319=LINE('',#12122,#2763);
#2320=LINE('',#12128,#2764);
#2321=LINE('',#12134,#2765);
#2322=LINE('',#12140,#2766);
#2323=LINE('',#12148,#2767);
#2324=LINE('',#12153,#2768);
#2762=VECTOR('',#9695,0.225);
#2763=VECTOR('',#9702,0.225);
#2764=VECTOR('',#9709,0.225);
#2765=VECTOR('',#9716,0.225);
#2766=VECTOR('',#9723,1.59);
#2767=VECTOR('',#9734,1.1);
#2768=VECTOR('',#9739,2.5);
#3215=CIRCLE('',#8356,0.225);
#3216=CIRCLE('',#8357,0.225);
#3217=CIRCLE('',#8359,0.225);
#3218=CIRCLE('',#8360,0.225);
#3219=CIRCLE('',#8362,0.225);
#3220=CIRCLE('',#8363,0.225);
#3221=CIRCLE('',#8365,0.225);
#3222=CIRCLE('',#8366,0.225);
#3223=CIRCLE('',#8368,1.59);
#3224=CIRCLE('',#8369,1.59);
#3225=CIRCLE('',#8371,1.1);
#3226=CIRCLE('',#8373,1.1);
#3227=CIRCLE('',#8375,2.5);
#3228=CIRCLE('',#8376,2.5);
#3695=VERTEX_POINT('',#12113);
#3696=VERTEX_POINT('',#12115);
#3697=VERTEX_POINT('',#12119);
#3698=VERTEX_POINT('',#12121);
#3699=VERTEX_POINT('',#12125);
#3700=VERTEX_POINT('',#12127);
#3701=VERTEX_POINT('',#12131);
#3702=VERTEX_POINT('',#12133);
#3703=VERTEX_POINT('',#12137);
#3704=VERTEX_POINT('',#12139);
#3705=VERTEX_POINT('',#12143);
#3706=VERTEX_POINT('',#12146);
#3707=VERTEX_POINT('',#12150);
#3708=VERTEX_POINT('',#12152);
#4413=EDGE_CURVE('',#3695,#3695,#3215,.T.);
#4414=EDGE_CURVE('',#3695,#3696,#2318,.T.);
#4415=EDGE_CURVE('',#3696,#3696,#3216,.T.);
#4416=EDGE_CURVE('',#3697,#3697,#3217,.T.);
#4417=EDGE_CURVE('',#3697,#3698,#2319,.T.);
#4418=EDGE_CURVE('',#3698,#3698,#3218,.T.);
#4419=EDGE_CURVE('',#3699,#3699,#3219,.T.);
#4420=EDGE_CURVE('',#3699,#3700,#2320,.T.);
#4421=EDGE_CURVE('',#3700,#3700,#3220,.T.);
#4422=EDGE_CURVE('',#3701,#3701,#3221,.T.);
#4423=EDGE_CURVE('',#3701,#3702,#2321,.T.);
#4424=EDGE_CURVE('',#3702,#3702,#3222,.T.);
#4425=EDGE_CURVE('',#3703,#3703,#3223,.T.);
#4426=EDGE_CURVE('',#3703,#3704,#2322,.T.);
#4427=EDGE_CURVE('',#3704,#3704,#3224,.T.);
#4428=EDGE_CURVE('',#3705,#3705,#3225,.T.);
#4429=EDGE_CURVE('',#3706,#3706,#3226,.T.);
#4430=EDGE_CURVE('',#3706,#3705,#2323,.T.);
#4431=EDGE_CURVE('',#3707,#3707,#3227,.T.);
#4432=EDGE_CURVE('',#3707,#3708,#2324,.T.);
#4433=EDGE_CURVE('',#3708,#3708,#3228,.T.);
#5574=ORIENTED_EDGE('',*,*,#4413,.F.);
#5575=ORIENTED_EDGE('',*,*,#4414,.T.);
#5576=ORIENTED_EDGE('',*,*,#4415,.F.);
#5577=ORIENTED_EDGE('',*,*,#4414,.F.);
#5578=ORIENTED_EDGE('',*,*,#4416,.F.);
#5579=ORIENTED_EDGE('',*,*,#4417,.T.);
#5580=ORIENTED_EDGE('',*,*,#4418,.F.);
#5581=ORIENTED_EDGE('',*,*,#4417,.F.);
#5582=ORIENTED_EDGE('',*,*,#4419,.F.);
#5583=ORIENTED_EDGE('',*,*,#4420,.T.);
#5584=ORIENTED_EDGE('',*,*,#4421,.F.);
#5585=ORIENTED_EDGE('',*,*,#4420,.F.);
#5586=ORIENTED_EDGE('',*,*,#4422,.F.);
#5587=ORIENTED_EDGE('',*,*,#4423,.T.);
#5588=ORIENTED_EDGE('',*,*,#4424,.F.);
#5589=ORIENTED_EDGE('',*,*,#4423,.F.);
#5590=ORIENTED_EDGE('',*,*,#4425,.F.);
#5591=ORIENTED_EDGE('',*,*,#4426,.T.);
#5592=ORIENTED_EDGE('',*,*,#4427,.T.);
#5593=ORIENTED_EDGE('',*,*,#4426,.F.);
#5594=ORIENTED_EDGE('',*,*,#4427,.F.);
#5595=ORIENTED_EDGE('',*,*,#4428,.F.);
#5596=ORIENTED_EDGE('',*,*,#4429,.F.);
#5597=ORIENTED_EDGE('',*,*,#4430,.T.);
#5598=ORIENTED_EDGE('',*,*,#4428,.T.);
#5599=ORIENTED_EDGE('',*,*,#4430,.F.);
#5600=ORIENTED_EDGE('',*,*,#4431,.F.);
#5601=ORIENTED_EDGE('',*,*,#4432,.T.);
#5602=ORIENTED_EDGE('',*,*,#4433,.T.);
#5603=ORIENTED_EDGE('',*,*,#4432,.F.);
#5604=ORIENTED_EDGE('',*,*,#4431,.T.);
#5605=ORIENTED_EDGE('',*,*,#4429,.T.);
#5606=ORIENTED_EDGE('',*,*,#4424,.T.);
#5607=ORIENTED_EDGE('',*,*,#4421,.T.);
#5608=ORIENTED_EDGE('',*,*,#4418,.T.);
#5609=ORIENTED_EDGE('',*,*,#4415,.T.);
#5610=ORIENTED_EDGE('',*,*,#4433,.F.);
#5611=ORIENTED_EDGE('',*,*,#4425,.T.);
#5612=ORIENTED_EDGE('',*,*,#4422,.T.);
#5613=ORIENTED_EDGE('',*,*,#4419,.T.);
#5614=ORIENTED_EDGE('',*,*,#4416,.T.);
#5615=ORIENTED_EDGE('',*,*,#4413,.T.);
#7097=CYLINDRICAL_SURFACE('',#8355,0.225);
#7098=CYLINDRICAL_SURFACE('',#8358,0.225);
#7099=CYLINDRICAL_SURFACE('',#8361,0.225);
#7100=CYLINDRICAL_SURFACE('',#8364,0.225);
#7101=CYLINDRICAL_SURFACE('',#8367,1.59);
#7102=CYLINDRICAL_SURFACE('',#8372,1.1);
#7103=CYLINDRICAL_SURFACE('',#8374,2.5);
#7300=ADVANCED_FACE('',(#1189),#7097,.F.);
#7301=ADVANCED_FACE('',(#1190),#7098,.F.);
#7302=ADVANCED_FACE('',(#1191),#7099,.F.);
#7303=ADVANCED_FACE('',(#1192),#7100,.F.);
#7304=ADVANCED_FACE('',(#1193),#7101,.T.);
#7305=ADVANCED_FACE('',(#1194,#733),#911,.F.);
#7306=ADVANCED_FACE('',(#1195),#7102,.F.);
#7307=ADVANCED_FACE('',(#1196),#7103,.T.);
#7308=ADVANCED_FACE('',(#1197,#734,#735,#736,#737,#738),#912,.T.);
#7309=ADVANCED_FACE('',(#1198,#739,#740,#741,#742,#743),#913,.F.);
#7661=CLOSED_SHELL('',(#7300,#7301,#7302,#7303,#7304,#7305,#7306,#7307,
#7308,#7309));
#8354=AXIS2_PLACEMENT_3D('',#12111,#9689,#9690);
#8355=AXIS2_PLACEMENT_3D('',#12112,#9691,#9692);
#8356=AXIS2_PLACEMENT_3D('',#12114,#9693,#9694);
#8357=AXIS2_PLACEMENT_3D('',#12117,#9696,#9697);
#8358=AXIS2_PLACEMENT_3D('',#12118,#9698,#9699);
#8359=AXIS2_PLACEMENT_3D('',#12120,#9700,#9701);
#8360=AXIS2_PLACEMENT_3D('',#12123,#9703,#9704);
#8361=AXIS2_PLACEMENT_3D('',#12124,#9705,#9706);
#8362=AXIS2_PLACEMENT_3D('',#12126,#9707,#9708);
#8363=AXIS2_PLACEMENT_3D('',#12129,#9710,#9711);
#8364=AXIS2_PLACEMENT_3D('',#12130,#9712,#9713);
#8365=AXIS2_PLACEMENT_3D('',#12132,#9714,#9715);
#8366=AXIS2_PLACEMENT_3D('',#12135,#9717,#9718);
#8367=AXIS2_PLACEMENT_3D('',#12136,#9719,#9720);
#8368=AXIS2_PLACEMENT_3D('',#12138,#9721,#9722);
#8369=AXIS2_PLACEMENT_3D('',#12141,#9724,#9725);
#8370=AXIS2_PLACEMENT_3D('',#12142,#9726,#9727);
#8371=AXIS2_PLACEMENT_3D('',#12144,#9728,#9729);
#8372=AXIS2_PLACEMENT_3D('',#12145,#9730,#9731);
#8373=AXIS2_PLACEMENT_3D('',#12147,#9732,#9733);
#8374=AXIS2_PLACEMENT_3D('',#12149,#9735,#9736);
#8375=AXIS2_PLACEMENT_3D('',#12151,#9737,#9738);
#8376=AXIS2_PLACEMENT_3D('',#12154,#9740,#9741);
#8377=AXIS2_PLACEMENT_3D('',#12155,#9742,#9743);
#8378=AXIS2_PLACEMENT_3D('',#12156,#9744,#9745);
#9689=DIRECTION('axis',(0.,0.,1.));
#9690=DIRECTION('refdir',(1.,0.,0.));
#9691=DIRECTION('center_axis',(0.,1.,0.));
#9692=DIRECTION('ref_axis',(1.,0.,0.));
#9693=DIRECTION('center_axis',(0.,1.,0.));
#9694=DIRECTION('ref_axis',(1.,0.,0.));
#9695=DIRECTION('',(0.,1.,0.));
#9696=DIRECTION('center_axis',(0.,-1.,0.));
#9697=DIRECTION('ref_axis',(1.,0.,0.));
#9698=DIRECTION('center_axis',(0.,1.,0.));
#9699=DIRECTION('ref_axis',(1.,0.,0.));
#9700=DIRECTION('center_axis',(0.,1.,0.));
#9701=DIRECTION('ref_axis',(1.,0.,0.));
#9702=DIRECTION('',(0.,1.,0.));
#9703=DIRECTION('center_axis',(0.,-1.,0.));
#9704=DIRECTION('ref_axis',(1.,0.,0.));
#9705=DIRECTION('center_axis',(0.,1.,0.));
#9706=DIRECTION('ref_axis',(1.,0.,0.));
#9707=DIRECTION('center_axis',(0.,1.,0.));
#9708=DIRECTION('ref_axis',(1.,0.,0.));
#9709=DIRECTION('',(0.,1.,0.));
#9710=DIRECTION('center_axis',(0.,-1.,0.));
#9711=DIRECTION('ref_axis',(1.,0.,0.));
#9712=DIRECTION('center_axis',(0.,1.,0.));
#9713=DIRECTION('ref_axis',(1.,0.,0.));
#9714=DIRECTION('center_axis',(0.,1.,0.));
#9715=DIRECTION('ref_axis',(1.,0.,0.));
#9716=DIRECTION('',(0.,1.,0.));
#9717=DIRECTION('center_axis',(0.,-1.,0.));
#9718=DIRECTION('ref_axis',(1.,0.,0.));
#9719=DIRECTION('center_axis',(0.,1.,0.));
#9720=DIRECTION('ref_axis',(1.,0.,0.));
#9721=DIRECTION('center_axis',(0.,1.,0.));
#9722=DIRECTION('ref_axis',(1.,0.,0.));
#9723=DIRECTION('',(0.,-1.,0.));
#9724=DIRECTION('center_axis',(0.,1.,0.));
#9725=DIRECTION('ref_axis',(1.,0.,0.));
#9726=DIRECTION('center_axis',(0.,1.,0.));
#9727=DIRECTION('ref_axis',(1.,0.,0.));
#9728=DIRECTION('center_axis',(0.,-1.,0.));
#9729=DIRECTION('ref_axis',(1.,0.,0.));
#9730=DIRECTION('center_axis',(0.,1.,0.));
#9731=DIRECTION('ref_axis',(1.,0.,0.));
#9732=DIRECTION('center_axis',(0.,-1.,0.));
#9733=DIRECTION('ref_axis',(1.,0.,0.));
#9734=DIRECTION('',(0.,-1.,0.));
#9735=DIRECTION('center_axis',(0.,1.,0.));
#9736=DIRECTION('ref_axis',(1.,0.,0.));
#9737=DIRECTION('center_axis',(0.,1.,0.));
#9738=DIRECTION('ref_axis',(1.,0.,0.));
#9739=DIRECTION('',(0.,-1.,0.));
#9740=DIRECTION('center_axis',(0.,1.,0.));
#9741=DIRECTION('ref_axis',(1.,0.,0.));
#9742=DIRECTION('center_axis',(0.,1.,0.));
#9743=DIRECTION('ref_axis',(1.,0.,0.));
#9744=DIRECTION('center_axis',(0.,1.,0.));
#9745=DIRECTION('ref_axis',(1.,0.,0.));
#12111=CARTESIAN_POINT('',(0.,0.,0.));
#12112=CARTESIAN_POINT('Origin',(-2.,7.7,7.));
#12113=CARTESIAN_POINT('',(-2.225,7.8,7.));
#12114=CARTESIAN_POINT('Origin',(-2.,7.8,7.));
#12115=CARTESIAN_POINT('',(-2.225,8.1,7.));
#12116=CARTESIAN_POINT('',(-2.225,7.7,7.));
#12117=CARTESIAN_POINT('Origin',(-2.,8.1,7.));
#12118=CARTESIAN_POINT('Origin',(1.22464679914735E-16,7.7,9.));
#12119=CARTESIAN_POINT('',(-0.225,7.8,9.));
#12120=CARTESIAN_POINT('Origin',(1.22464679914735E-16,7.8,9.));
#12121=CARTESIAN_POINT('',(-0.225,8.1,9.));
#12122=CARTESIAN_POINT('',(-0.225,7.7,9.));
#12123=CARTESIAN_POINT('Origin',(1.22464679914735E-16,8.1,9.));
#12124=CARTESIAN_POINT('Origin',(2.,7.7,7.));
#12125=CARTESIAN_POINT('',(1.775,7.8,7.));
#12126=CARTESIAN_POINT('Origin',(2.,7.8,7.));
#12127=CARTESIAN_POINT('',(1.775,8.1,7.));
#12128=CARTESIAN_POINT('',(1.775,7.7,7.));
#12129=CARTESIAN_POINT('Origin',(2.,8.1,7.));
#12130=CARTESIAN_POINT('Origin',(-3.67394039744206E-16,7.7,5.));
#12131=CARTESIAN_POINT('',(-0.225,7.8,5.));
#12132=CARTESIAN_POINT('Origin',(-3.67394039744206E-16,7.8,5.));
#12133=CARTESIAN_POINT('',(-0.225,8.1,5.));
#12134=CARTESIAN_POINT('',(-0.225,7.7,5.));
#12135=CARTESIAN_POINT('Origin',(-3.67394039744206E-16,8.1,5.));
#12136=CARTESIAN_POINT('Origin',(0.,7.5,7.));
#12137=CARTESIAN_POINT('',(-1.59,7.8,7.));
#12138=CARTESIAN_POINT('Origin',(0.,7.8,7.));
#12139=CARTESIAN_POINT('',(-1.59,7.5,7.));
#12140=CARTESIAN_POINT('',(-1.59,7.5,7.));
#12141=CARTESIAN_POINT('Origin',(0.,7.5,7.));
#12142=CARTESIAN_POINT('Origin',(0.,7.5,7.));
#12143=CARTESIAN_POINT('',(-1.1,7.5,7.));
#12144=CARTESIAN_POINT('Origin',(0.,7.5,7.));
#12145=CARTESIAN_POINT('Origin',(0.,7.8,7.));
#12146=CARTESIAN_POINT('',(-1.1,8.1,7.));
#12147=CARTESIAN_POINT('Origin',(0.,8.1,7.));
#12148=CARTESIAN_POINT('',(-1.1,7.8,7.));
#12149=CARTESIAN_POINT('Origin',(0.,7.8,7.));
#12150=CARTESIAN_POINT('',(-2.5,8.1,7.));
#12151=CARTESIAN_POINT('Origin',(0.,8.1,7.));
#12152=CARTESIAN_POINT('',(-2.5,7.8,7.));
#12153=CARTESIAN_POINT('',(-2.5,7.8,7.));
#12154=CARTESIAN_POINT('Origin',(0.,7.8,7.));
#12155=CARTESIAN_POINT('Origin',(0.,8.1,7.));
#12156=CARTESIAN_POINT('Origin',(0.,7.8,7.));
#14741=UNCERTAINTY_MEASURE_WITH_UNIT(LENGTH_MEASURE(0.001),#14823,
'DISTANCE_ACCURACY_VALUE',
'Maximum model space distance between geometric entities at asserted c
onnectivities');
#14777=UNCERTAINTY_MEASURE_WITH_UNIT(LENGTH_MEASURE(0.001),#14823,
'DISTANCE_ACCURACY_VALUE',
'Maximum model space distance between geometric entities at asserted c
onnectivities');
#14786=(
GEOMETRIC_REPRESENTATION_CONTEXT(3)
GLOBAL_UNCERTAINTY_ASSIGNED_CONTEXT((#14741))
GLOBAL_UNIT_ASSIGNED_CONTEXT((#14823,#14825,#14826))
REPRESENTATION_CONTEXT('','3D')
);
#14822=(
GEOMETRIC_REPRESENTATION_CONTEXT(3)
GLOBAL_UNCERTAINTY_ASSIGNED_CONTEXT((#14777))
GLOBAL_UNIT_ASSIGNED_CONTEXT((#14823,#14825,#14826))
REPRESENTATION_CONTEXT('','3D')
);
#14823=(
LENGTH_UNIT()
NAMED_UNIT(*)
SI_UNIT(.CENTI.,.METRE.)
);
#14825=(
NAMED_UNIT(*)
PLANE_ANGLE_UNIT()
SI_UNIT($,.RADIAN.)
);
#14826=(
NAMED_UNIT(*)
SI_UNIT($,.STERADIAN.)
SOLID_ANGLE_UNIT()
);
#14835=SHAPE_DEFINITION_REPRESENTATION(#14879,#15006);
#14879=PRODUCT_DEFINITION_SHAPE('',$,#15051);
#15006=SHAPE_REPRESENTATION('',(#8354),#14786);
#15042=PRODUCT_DEFINITION_CONTEXT('part definition',#15176,'design');
#15051=PRODUCT_DEFINITION('Support cap (3)','Support cap (3)',#15095,#15042);
#15095=PRODUCT_DEFINITION_FORMATION('',$,#15186);
#15176=APPLICATION_CONTEXT(
'Core Data for Automotive Mechanical Design Process');
#15177=PRODUCT_CONTEXT('part definition',#15176,'mechanical');
#15186=PRODUCT('Support cap (3)','Support cap (3)','Support cap (3)',(#15177));
#15271=COLOUR_RGB('Sky Blue',0.24,0.69,0.87);
#15272=FILL_AREA_STYLE_COLOUR('',#15271);
#15273=FILL_AREA_STYLE('',(#15272));
#15274=SURFACE_STYLE_FILL_AREA(#15273);
#15275=SURFACE_SIDE_STYLE('',(#15274));
#15276=SURFACE_STYLE_USAGE(.BOTH.,#15275);
#15277=PRESENTATION_STYLE_ASSIGNMENT((#15276));
ENDSEC;
END-ISO-10303-21;
